ISO-10303-21;
HEADER;
/* Generated by software containing ST-Developer
 * from STEP Tools, Inc. (www.steptools.com) 
 */

FILE_DESCRIPTION(
/* description */ ('Hand-operated arbor press'),
/* implementation_level */ '2;1');

FILE_NAME(
/* name */ 'Cap Screw - M6x25.step',
/* time_stamp */ '2026-10-28T03:25:25-07:00',
/* author */ (''),
/* organization */ (''),
/* preprocessor_version */ 'ST-DEVELOPER v20.2',
/* originating_system */ 'Autodesk Translation Framework v15.17.0.0',
/* authorisation */ '');

FILE_SCHEMA (('AUTOMOTIVE_DESIGN { 1 0 10303 214 3 1 1 }'));
ENDSEC;

DATA;
#10=MECHANICAL_DESIGN_GEOMETRIC_PRESENTATION_REPRESENTATION('',(#632),#32751);
#475=ORIENTED_CLOSED_SHELL('',*,#12532,.F.);
#490=CONICAL_SURFACE('',#14028,0.475,0.785398163397449);
#491=CONICAL_SURFACE('',#14032,0.485,0.785398163397448);
#492=CONICAL_SURFACE('',#14036,0.31,0.463647609000806);
#493=CONICAL_SURFACE('',#14040,0.27,0.785398163397448);
#500=BREP_WITH_VOIDS('Body1',#12531,(#475));
#541=SHAPE_REPRESENTATION_RELATIONSHIP('SRR','None',#32973,#583);
#583=ADVANCED_BREP_SHAPE_REPRESENTATION('',(#500),#32747);
#632=STYLED_ITEM('',(#33249),#500);
#845=FACE_BOUND('',#2787,.T.);
#1269=PLANE('',#14026);
#1270=PLANE('',#14034);
#1271=PLANE('',#14042);
#1272=PLANE('',#14043);
#1273=PLANE('',#14044);
#1274=PLANE('',#14045);
#1275=PLANE('',#14046);
#1276=PLANE('',#14047);
#1277=PLANE('',#14048);
#1278=PLANE('',#14049);
#1279=PLANE('',#14050);
#1936=FACE_OUTER_BOUND('',#2782,.T.);
#1937=FACE_OUTER_BOUND('',#2783,.T.);
#1938=FACE_OUTER_BOUND('',#2784,.T.);
#1939=FACE_OUTER_BOUND('',#2785,.T.);
#1940=FACE_OUTER_BOUND('',#2786,.T.);
#1941=FACE_OUTER_BOUND('',#2788,.T.);
#1942=FACE_OUTER_BOUND('',#2789,.T.);
#1943=FACE_OUTER_BOUND('',#2790,.T.);
#1944=FACE_OUTER_BOUND('',#2791,.T.);
#1945=FACE_OUTER_BOUND('',#2792,.T.);
#1946=FACE_OUTER_BOUND('',#2793,.T.);
#1947=FACE_OUTER_BOUND('',#2794,.T.);
#1948=FACE_OUTER_BOUND('',#2795,.T.);
#1949=FACE_OUTER_BOUND('',#2796,.T.);
#1950=FACE_OUTER_BOUND('',#2797,.T.);
#1951=FACE_OUTER_BOUND('',#2798,.T.);
#1952=FACE_OUTER_BOUND('',#2799,.T.);
#2782=EDGE_LOOP('',(#11502));
#2783=EDGE_LOOP('',(#11503,#11504,#11505,#11506));
#2784=EDGE_LOOP('',(#11507,#11508,#11509,#11510));
#2785=EDGE_LOOP('',(#11511,#11512,#11513,#11514));
#2786=EDGE_LOOP('',(#11515));
#2787=EDGE_LOOP('',(#11516));
#2788=EDGE_LOOP('',(#11517,#11518,#11519,#11520));
#2789=EDGE_LOOP('',(#11521,#11522,#11523,#11524));
#2790=EDGE_LOOP('',(#11525,#11526,#11527,#11528));
#2791=EDGE_LOOP('',(#11529));
#2792=EDGE_LOOP('',(#11530,#11531,#11532,#11533));
#2793=EDGE_LOOP('',(#11534,#11535,#11536,#11537));
#2794=EDGE_LOOP('',(#11538,#11539,#11540,#11541));
#2795=EDGE_LOOP('',(#11542,#11543,#11544,#11545));
#2796=EDGE_LOOP('',(#11546,#11547,#11548,#11549));
#2797=EDGE_LOOP('',(#11550,#11551,#11552,#11553));
#2798=EDGE_LOOP('',(#11554,#11555,#11556,#11557,#11558,#11559));
#2799=EDGE_LOOP('',(#11560,#11561,#11562,#11563,#11564,#11565));
#3945=LINE('',#32437,#5116);
#3946=LINE('',#32441,#5117);
#3947=LINE('',#32445,#5118);
#3948=LINE('',#32452,#5119);
#3949=LINE('',#32456,#5120);
#3950=LINE('',#32460,#5121);
#3951=LINE('',#32465,#5122);
#3952=LINE('',#32467,#5123);
#3953=LINE('',#32469,#5124);
#3954=LINE('',#32470,#5125);
#3955=LINE('',#32473,#5126);
#3956=LINE('',#32475,#5127);
#3957=LINE('',#32476,#5128);
#3958=LINE('',#32479,#5129);
#3959=LINE('',#32481,#5130);
#3960=LINE('',#32482,#5131);
#3961=LINE('',#32485,#5132);
#3962=LINE('',#32487,#5133);
#3963=LINE('',#32488,#5134);
#3964=LINE('',#32491,#5135);
#3965=LINE('',#32493,#5136);
#3966=LINE('',#32494,#5137);
#3967=LINE('',#32496,#5138);
#3968=LINE('',#32497,#5139);
#5116=VECTOR('',#17338,0.475);
#5117=VECTOR('',#17343,0.5);
#5118=VECTOR('',#17348,0.485);
#5119=VECTOR('',#17357,0.31);
#5120=VECTOR('',#17362,0.3);
#5121=VECTOR('',#17367,0.27);
#5122=VECTOR('',#17372,1.);
#5123=VECTOR('',#17373,1.);
#5124=VECTOR('',#17374,1.);
#5125=VECTOR('',#17375,1.);
#5126=VECTOR('',#17378,1.);
#5127=VECTOR('',#17379,1.);
#5128=VECTOR('',#17380,1.);
#5129=VECTOR('',#17383,1.);
#5130=VECTOR('',#17384,1.);
#5131=VECTOR('',#17385,1.);
#5132=VECTOR('',#17388,1.);
#5133=VECTOR('',#17389,1.);
#5134=VECTOR('',#17390,1.);
#5135=VECTOR('',#17393,1.);
#5136=VECTOR('',#17394,1.);
#5137=VECTOR('',#17395,1.);
#5138=VECTOR('',#17398,1.);
#5139=VECTOR('',#17399,1.);
#5536=CIRCLE('',#14027,0.45);
#5537=CIRCLE('',#14029,0.5);
#5538=CIRCLE('',#14031,0.5);
#5539=CIRCLE('',#14033,0.47);
#5540=CIRCLE('',#14035,0.32);
#5541=CIRCLE('',#14037,0.2942);
#5542=CIRCLE('',#14039,0.2942);
#5543=CIRCLE('',#14041,0.24);
#6621=VERTEX_POINT('',#32432);
#6622=VERTEX_POINT('',#32435);
#6623=VERTEX_POINT('',#32439);
#6624=VERTEX_POINT('',#32443);
#6625=VERTEX_POINT('',#32447);
#6626=VERTEX_POINT('',#32450);
#6627=VERTEX_POINT('',#32454);
#6628=VERTEX_POINT('',#32458);
#6629=VERTEX_POINT('',#32463);
#6630=VERTEX_POINT('',#32464);
#6631=VERTEX_POINT('',#32466);
#6632=VERTEX_POINT('',#32468);
#6633=VERTEX_POINT('',#32472);
#6634=VERTEX_POINT('',#32474);
#6635=VERTEX_POINT('',#32478);
#6636=VERTEX_POINT('',#32480);
#6637=VERTEX_POINT('',#32484);
#6638=VERTEX_POINT('',#32486);
#6639=VERTEX_POINT('',#32490);
#6640=VERTEX_POINT('',#32492);
#8254=EDGE_CURVE('',#6621,#6621,#5536,.T.);
#8255=EDGE_CURVE('',#6622,#6622,#5537,.T.);
#8256=EDGE_CURVE('',#6622,#6621,#3945,.T.);
#8257=EDGE_CURVE('',#6623,#6623,#5538,.T.);
#8258=EDGE_CURVE('',#6623,#6622,#3946,.T.);
#8259=EDGE_CURVE('',#6624,#6624,#5539,.T.);
#8260=EDGE_CURVE('',#6624,#6623,#3947,.T.);
#8261=EDGE_CURVE('',#6625,#6625,#5540,.T.);
#8262=EDGE_CURVE('',#6626,#6626,#5541,.F.);
#8263=EDGE_CURVE('',#6626,#6625,#3948,.T.);
#8264=EDGE_CURVE('',#6627,#6627,#5542,.F.);
#8265=EDGE_CURVE('',#6627,#6626,#3949,.T.);
#8266=EDGE_CURVE('',#6628,#6628,#5543,.T.);
#8267=EDGE_CURVE('',#6628,#6627,#3950,.T.);
#8268=EDGE_CURVE('',#6629,#6630,#3951,.T.);
#8269=EDGE_CURVE('',#6630,#6631,#3952,.T.);
#8270=EDGE_CURVE('',#6631,#6632,#3953,.T.);
#8271=EDGE_CURVE('',#6629,#6632,#3954,.T.);
#8272=EDGE_CURVE('',#6630,#6633,#3955,.T.);
#8273=EDGE_CURVE('',#6633,#6634,#3956,.T.);
#8274=EDGE_CURVE('',#6634,#6631,#3957,.T.);
#8275=EDGE_CURVE('',#6633,#6635,#3958,.T.);
#8276=EDGE_CURVE('',#6635,#6636,#3959,.T.);
#8277=EDGE_CURVE('',#6636,#6634,#3960,.T.);
#8278=EDGE_CURVE('',#6635,#6637,#3961,.T.);
#8279=EDGE_CURVE('',#6637,#6638,#3962,.T.);
#8280=EDGE_CURVE('',#6638,#6636,#3963,.T.);
#8281=EDGE_CURVE('',#6637,#6639,#3964,.T.);
#8282=EDGE_CURVE('',#6639,#6640,#3965,.T.);
#8283=EDGE_CURVE('',#6640,#6638,#3966,.T.);
#8284=EDGE_CURVE('',#6639,#6629,#3967,.T.);
#8285=EDGE_CURVE('',#6632,#6640,#3968,.T.);
#11502=ORIENTED_EDGE('',*,*,#8254,.F.);
#11503=ORIENTED_EDGE('',*,*,#8255,.F.);
#11504=ORIENTED_EDGE('',*,*,#8256,.T.);
#11505=ORIENTED_EDGE('',*,*,#8254,.T.);
#11506=ORIENTED_EDGE('',*,*,#8256,.F.);
#11507=ORIENTED_EDGE('',*,*,#8257,.F.);
#11508=ORIENTED_EDGE('',*,*,#8258,.T.);
#11509=ORIENTED_EDGE('',*,*,#8255,.T.);
#11510=ORIENTED_EDGE('',*,*,#8258,.F.);
#11511=ORIENTED_EDGE('',*,*,#8259,.F.);
#11512=ORIENTED_EDGE('',*,*,#8260,.T.);
#11513=ORIENTED_EDGE('',*,*,#8257,.T.);
#11514=ORIENTED_EDGE('',*,*,#8260,.F.);
#11515=ORIENTED_EDGE('',*,*,#8259,.T.);
#11516=ORIENTED_EDGE('',*,*,#8261,.F.);
#11517=ORIENTED_EDGE('',*,*,#8262,.F.);
#11518=ORIENTED_EDGE('',*,*,#8263,.T.);
#11519=ORIENTED_EDGE('',*,*,#8261,.T.);
#11520=ORIENTED_EDGE('',*,*,#8263,.F.);
#11521=ORIENTED_EDGE('',*,*,#8264,.F.);
#11522=ORIENTED_EDGE('',*,*,#8265,.T.);
#11523=ORIENTED_EDGE('',*,*,#8262,.T.);
#11524=ORIENTED_EDGE('',*,*,#8265,.F.);
#11525=ORIENTED_EDGE('',*,*,#8266,.F.);
#11526=ORIENTED_EDGE('',*,*,#8267,.T.);
#11527=ORIENTED_EDGE('',*,*,#8264,.T.);
#11528=ORIENTED_EDGE('',*,*,#8267,.F.);
#11529=ORIENTED_EDGE('',*,*,#8266,.T.);
#11530=ORIENTED_EDGE('',*,*,#8268,.T.);
#11531=ORIENTED_EDGE('',*,*,#8269,.T.);
#11532=ORIENTED_EDGE('',*,*,#8270,.T.);
#11533=ORIENTED_EDGE('',*,*,#8271,.F.);
#11534=ORIENTED_EDGE('',*,*,#8272,.T.);
#11535=ORIENTED_EDGE('',*,*,#8273,.T.);
#11536=ORIENTED_EDGE('',*,*,#8274,.T.);
#11537=ORIENTED_EDGE('',*,*,#8269,.F.);
#11538=ORIENTED_EDGE('',*,*,#8275,.T.);
#11539=ORIENTED_EDGE('',*,*,#8276,.T.);
#11540=ORIENTED_EDGE('',*,*,#8277,.T.);
#11541=ORIENTED_EDGE('',*,*,#8273,.F.);
#11542=ORIENTED_EDGE('',*,*,#8278,.T.);
#11543=ORIENTED_EDGE('',*,*,#8279,.T.);
#11544=ORIENTED_EDGE('',*,*,#8280,.T.);
#11545=ORIENTED_EDGE('',*,*,#8276,.F.);
#11546=ORIENTED_EDGE('',*,*,#8281,.T.);
#11547=ORIENTED_EDGE('',*,*,#8282,.T.);
#11548=ORIENTED_EDGE('',*,*,#8283,.T.);
#11549=ORIENTED_EDGE('',*,*,#8279,.F.);
#11550=ORIENTED_EDGE('',*,*,#8284,.T.);
#11551=ORIENTED_EDGE('',*,*,#8271,.T.);
#11552=ORIENTED_EDGE('',*,*,#8285,.T.);
#11553=ORIENTED_EDGE('',*,*,#8282,.F.);
#11554=ORIENTED_EDGE('',*,*,#8284,.F.);
#11555=ORIENTED_EDGE('',*,*,#8281,.F.);
#11556=ORIENTED_EDGE('',*,*,#8278,.F.);
#11557=ORIENTED_EDGE('',*,*,#8275,.F.);
#11558=ORIENTED_EDGE('',*,*,#8272,.F.);
#11559=ORIENTED_EDGE('',*,*,#8268,.F.);
#11560=ORIENTED_EDGE('',*,*,#8285,.F.);
#11561=ORIENTED_EDGE('',*,*,#8270,.F.);
#11562=ORIENTED_EDGE('',*,*,#8274,.F.);
#11563=ORIENTED_EDGE('',*,*,#8277,.F.);
#11564=ORIENTED_EDGE('',*,*,#8280,.F.);
#11565=ORIENTED_EDGE('',*,*,#8283,.F.);
#11796=CYLINDRICAL_SURFACE('',#14030,0.5);
#11797=CYLINDRICAL_SURFACE('',#14038,0.2942);
#12445=ADVANCED_FACE('',(#1936),#1269,.T.);
#12446=ADVANCED_FACE('',(#1937),#490,.T.);
#12447=ADVANCED_FACE('',(#1938),#11796,.T.);
#12448=ADVANCED_FACE('',(#1939),#491,.T.);
#12449=ADVANCED_FACE('',(#1940,#845),#1270,.T.);
#12450=ADVANCED_FACE('',(#1941),#492,.T.);
#12451=ADVANCED_FACE('',(#1942),#11797,.T.);
#12452=ADVANCED_FACE('',(#1943),#493,.T.);
#12453=ADVANCED_FACE('',(#1944),#1271,.T.);
#12454=ADVANCED_FACE('',(#1945),#1272,.F.);
#12455=ADVANCED_FACE('',(#1946),#1273,.F.);
#12456=ADVANCED_FACE('',(#1947),#1274,.F.);
#12457=ADVANCED_FACE('',(#1948),#1275,.F.);
#12458=ADVANCED_FACE('',(#1949),#1276,.F.);
#12459=ADVANCED_FACE('',(#1950),#1277,.F.);
#12460=ADVANCED_FACE('',(#1951),#1278,.F.);
#12461=ADVANCED_FACE('',(#1952),#1279,.F.);
#12531=CLOSED_SHELL('',(#12445,#12446,#12447,#12448,#12449,#12450,#12451,
#12452,#12453));
#12532=CLOSED_SHELL('',(#12454,#12455,#12456,#12457,#12458,#12459,#12460,
#12461));
#14025=AXIS2_PLACEMENT_3D('',#32430,#17328,#17329);
#14026=AXIS2_PLACEMENT_3D('',#32431,#17330,#17331);
#14027=AXIS2_PLACEMENT_3D('',#32433,#17332,#17333);
#14028=AXIS2_PLACEMENT_3D('',#32434,#17334,#17335);
#14029=AXIS2_PLACEMENT_3D('',#32436,#17336,#17337);
#14030=AXIS2_PLACEMENT_3D('',#32438,#17339,#17340);
#14031=AXIS2_PLACEMENT_3D('',#32440,#17341,#17342);
#14032=AXIS2_PLACEMENT_3D('',#32442,#17344,#17345);
#14033=AXIS2_PLACEMENT_3D('',#32444,#17346,#17347);
#14034=AXIS2_PLACEMENT_3D('',#32446,#17349,#17350);
#14035=AXIS2_PLACEMENT_3D('',#32448,#17351,#17352);
#14036=AXIS2_PLACEMENT_3D('',#32449,#17353,#17354);
#14037=AXIS2_PLACEMENT_3D('',#32451,#17355,#17356);
#14038=AXIS2_PLACEMENT_3D('',#32453,#17358,#17359);
#14039=AXIS2_PLACEMENT_3D('',#32455,#17360,#17361);
#14040=AXIS2_PLACEMENT_3D('',#32457,#17363,#17364);
#14041=AXIS2_PLACEMENT_3D('',#32459,#17365,#17366);
#14042=AXIS2_PLACEMENT_3D('',#32461,#17368,#17369);
#14043=AXIS2_PLACEMENT_3D('',#32462,#17370,#17371);
#14044=AXIS2_PLACEMENT_3D('',#32471,#17376,#17377);
#14045=AXIS2_PLACEMENT_3D('',#32477,#17381,#17382);
#14046=AXIS2_PLACEMENT_3D('',#32483,#17386,#17387);
#14047=AXIS2_PLACEMENT_3D('',#32489,#17391,#17392);
#14048=AXIS2_PLACEMENT_3D('',#32495,#17396,#17397);
#14049=AXIS2_PLACEMENT_3D('',#32498,#17400,#17401);
#14050=AXIS2_PLACEMENT_3D('',#32499,#17402,#17403);
#17328=DIRECTION('axis',(0.,0.,1.));
#17329=DIRECTION('refdir',(1.,0.,0.));
#17330=DIRECTION('center_axis',(0.,1.,0.));
#17331=DIRECTION('ref_axis',(0.,0.,1.));
#17332=DIRECTION('center_axis',(0.,-1.,0.));
#17333=DIRECTION('ref_axis',(1.,0.,0.));
#17334=DIRECTION('center_axis',(0.,-1.,0.));
#17335=DIRECTION('ref_axis',(1.,0.,0.));
#17336=DIRECTION('center_axis',(0.,-1.,0.));
#17337=DIRECTION('ref_axis',(1.,0.,0.));
#17338=DIRECTION('',(0.707106781186548,0.707106781186547,8.65956056235494E-17));
#17339=DIRECTION('center_axis',(0.,-1.,0.));
#17340=DIRECTION('ref_axis',(1.,0.,0.));
#17341=DIRECTION('center_axis',(0.,-1.,0.));
#17342=DIRECTION('ref_axis',(1.,0.,0.));
#17343=DIRECTION('',(0.,1.,0.));
#17344=DIRECTION('center_axis',(0.,1.,0.));
#17345=DIRECTION('ref_axis',(1.,0.,0.));
#17346=DIRECTION('center_axis',(0.,-1.,0.));
#17347=DIRECTION('ref_axis',(1.,0.,0.));
#17348=DIRECTION('',(-0.707106781186547,0.707106781186548,-8.65956056235493E-17));
#17349=DIRECTION('center_axis',(0.,-1.,0.));
#17350=DIRECTION('ref_axis',(0.,0.,-1.));
#17351=DIRECTION('center_axis',(0.,-1.,0.));
#17352=DIRECTION('ref_axis',(1.,0.,0.));
#17353=DIRECTION('center_axis',(0.,1.,0.));
#17354=DIRECTION('ref_axis',(1.,0.,0.));
#17355=DIRECTION('center_axis',(0.,1.,0.));
#17356=DIRECTION('ref_axis',(1.,0.,0.));
#17357=DIRECTION('',(-0.447213595499958,0.894427190999916,-5.47678698264203E-17));
#17358=DIRECTION('center_axis',(0.,-1.,0.));
#17359=DIRECTION('ref_axis',(1.,0.,0.));
#17360=DIRECTION('center_axis',(0.,1.,0.));
#17361=DIRECTION('ref_axis',(1.,0.,0.));
#17362=DIRECTION('',(0.,1.,0.));
#17363=DIRECTION('center_axis',(0.,1.,0.));
#17364=DIRECTION('ref_axis',(1.,0.,0.));
#17365=DIRECTION('center_axis',(0.,-1.,0.));
#17366=DIRECTION('ref_axis',(1.,0.,0.));
#17367=DIRECTION('',(-0.707106781186547,0.707106781186548,-8.65956056235493E-17));
#17368=DIRECTION('center_axis',(0.,-1.,0.));
#17369=DIRECTION('ref_axis',(0.,0.,-1.));
#17370=DIRECTION('center_axis',(0.866025403784439,0.,-0.5));
#17371=DIRECTION('ref_axis',(0.5,0.,0.866025403784439));
#17372=DIRECTION('',(-0.5,0.,-0.866025403784439));
#17373=DIRECTION('',(0.,-1.,0.));
#17374=DIRECTION('',(0.5,0.,0.866025403784439));
#17375=DIRECTION('',(0.,-1.,0.));
#17376=DIRECTION('center_axis',(1.92296268638356E-16,0.,-1.));
#17377=DIRECTION('ref_axis',(1.,0.,1.92296268638356E-16));
#17378=DIRECTION('',(-1.,0.,-1.92296268638356E-16));
#17379=DIRECTION('',(0.,-1.,0.));
#17380=DIRECTION('',(1.,0.,1.92296268638356E-16));
#17381=DIRECTION('center_axis',(-0.866025403784439,0.,-0.5));
#17382=DIRECTION('ref_axis',(0.5,0.,-0.866025403784439));
#17383=DIRECTION('',(-0.5,0.,0.866025403784438));
#17384=DIRECTION('',(0.,-1.,0.));
#17385=DIRECTION('',(0.5,0.,-0.866025403784438));
#17386=DIRECTION('center_axis',(-0.866025403784439,0.,0.5));
#17387=DIRECTION('ref_axis',(-0.5,0.,-0.866025403784439));
#17388=DIRECTION('',(0.5,0.,0.866025403784439));
#17389=DIRECTION('',(0.,-1.,0.));
#17390=DIRECTION('',(-0.5,0.,-0.866025403784439));
#17391=DIRECTION('center_axis',(-1.92296268638356E-16,0.,1.));
#17392=DIRECTION('ref_axis',(-1.,0.,-1.92296268638356E-16));
#17393=DIRECTION('',(1.,0.,1.92296268638356E-16));
#17394=DIRECTION('',(0.,-1.,0.));
#17395=DIRECTION('',(-1.,0.,-1.92296268638356E-16));
#17396=DIRECTION('center_axis',(0.866025403784439,0.,0.5));
#17397=DIRECTION('ref_axis',(-0.5,0.,0.866025403784439));
#17398=DIRECTION('',(0.5,0.,-0.866025403784439));
#17399=DIRECTION('',(-0.5,0.,0.866025403784439));
#17400=DIRECTION('center_axis',(0.,1.,0.));
#17401=DIRECTION('ref_axis',(1.,0.,0.));
#17402=DIRECTION('center_axis',(0.,-1.,0.));
#17403=DIRECTION('ref_axis',(0.,0.,-1.));
#32430=CARTESIAN_POINT('',(0.,0.,0.));
#32431=CARTESIAN_POINT('Origin',(0.45,0.6,0.));
#32432=CARTESIAN_POINT('',(-0.45,0.6,-5.51091059616309E-17));
#32433=CARTESIAN_POINT('Origin',(0.,0.6,0.));
#32434=CARTESIAN_POINT('Origin',(0.,0.575,0.));
#32435=CARTESIAN_POINT('',(-0.5,0.55,-6.12323399573677E-17));
#32436=CARTESIAN_POINT('Origin',(0.,0.55,0.));
#32437=CARTESIAN_POINT('',(-0.475,0.575,-5.81707229594993E-17));
#32438=CARTESIAN_POINT('Origin',(0.,0.29,0.));
#32439=CARTESIAN_POINT('',(-0.5,0.0299999999999998,-6.12323399573677E-17));
#32440=CARTESIAN_POINT('Origin',(0.,0.0299999999999998,0.));
#32441=CARTESIAN_POINT('',(-0.5,0.29,-6.12323399573677E-17));
#32442=CARTESIAN_POINT('Origin',(0.,0.0150000000000001,0.));
#32443=CARTESIAN_POINT('',(-0.47,7.11236625150491E-17,-5.75583995599256E-17));
#32444=CARTESIAN_POINT('Origin',(0.,0.,0.));
#32445=CARTESIAN_POINT('',(-0.485,0.0150000000000001,-5.93953697586466E-17));
#32446=CARTESIAN_POINT('Origin',(0.32,0.,0.));
#32447=CARTESIAN_POINT('',(-0.32,-6.93889390390723E-18,-3.91886975727153E-17));
#32448=CARTESIAN_POINT('Origin',(0.,0.,0.));
#32449=CARTESIAN_POINT('Origin',(0.,-0.02,0.));
#32450=CARTESIAN_POINT('',(-0.2942,-0.0515999999999999,3.60291088309151E-17));
#32451=CARTESIAN_POINT('Origin',(0.,-0.0515999999999999,0.));
#32452=CARTESIAN_POINT('',(-0.31,-0.02,-3.7964050773568E-17));
#32453=CARTESIAN_POINT('Origin',(0.,-1.24,0.));
#32454=CARTESIAN_POINT('',(-0.2942,-2.4458,3.60291088309151E-17));
#32455=CARTESIAN_POINT('Origin',(0.,-2.4458,0.));
#32456=CARTESIAN_POINT('',(-0.2942,-1.24,-3.60291088309151E-17));
#32457=CARTESIAN_POINT('Origin',(0.,-2.47,0.));
#32458=CARTESIAN_POINT('',(-0.24,-2.5,-2.93915231795365E-17));
#32459=CARTESIAN_POINT('Origin',(0.,-2.5,0.));
#32460=CARTESIAN_POINT('',(-0.27,-2.47,-3.30654635769785E-17));
#32461=CARTESIAN_POINT('Origin',(0.,-2.5,0.));
#32462=CARTESIAN_POINT('Origin',(0.144337567297406,-0.6,-0.25));
#32463=CARTESIAN_POINT('',(0.288675134594813,-0.6,0.));
#32464=CARTESIAN_POINT('',(0.144337567297406,-0.6,-0.25));
#32465=CARTESIAN_POINT('',(0.288675134594813,-0.6,0.));
#32466=CARTESIAN_POINT('',(0.144337567297406,-0.96,-0.25));
#32467=CARTESIAN_POINT('',(0.144337567297406,-0.6,-0.25));
#32468=CARTESIAN_POINT('',(0.288675134594813,-0.96,0.));
#32469=CARTESIAN_POINT('',(0.288675134594813,-0.96,0.));
#32470=CARTESIAN_POINT('',(0.288675134594813,-0.6,0.));
#32471=CARTESIAN_POINT('Origin',(-0.144337567297406,-0.6,-0.25));
#32472=CARTESIAN_POINT('',(-0.144337567297406,-0.6,-0.25));
#32473=CARTESIAN_POINT('',(0.144337567297406,-0.6,-0.25));
#32474=CARTESIAN_POINT('',(-0.144337567297406,-0.96,-0.25));
#32475=CARTESIAN_POINT('',(-0.144337567297406,-0.6,-0.25));
#32476=CARTESIAN_POINT('',(0.144337567297406,-0.96,-0.25));
#32477=CARTESIAN_POINT('Origin',(-0.288675134594813,-0.6,-8.32667268468867E-17));
#32478=CARTESIAN_POINT('',(-0.288675134594813,-0.6,-3.53525079574969E-17));
#32479=CARTESIAN_POINT('',(-0.144337567297406,-0.6,-0.25));
#32480=CARTESIAN_POINT('',(-0.288675134594813,-0.96,-5.55111512312578E-17));
#32481=CARTESIAN_POINT('',(-0.288675134594813,-0.6,-3.53525079574969E-17));
#32482=CARTESIAN_POINT('',(-0.144337567297406,-0.96,-0.25));
#32483=CARTESIAN_POINT('Origin',(-0.144337567297407,-0.6,0.25));
#32484=CARTESIAN_POINT('',(-0.144337567297407,-0.6,0.25));
#32485=CARTESIAN_POINT('',(-0.288675134594813,-0.6,-3.53525079574969E-17));
#32486=CARTESIAN_POINT('',(-0.144337567297407,-0.96,0.25));
#32487=CARTESIAN_POINT('',(-0.144337567297407,-0.6,0.25));
#32488=CARTESIAN_POINT('',(-0.288675134594813,-0.96,-3.53525079574969E-17));
#32489=CARTESIAN_POINT('Origin',(0.144337567297406,-0.6,0.25));
#32490=CARTESIAN_POINT('',(0.144337567297406,-0.6,0.25));
#32491=CARTESIAN_POINT('',(-0.144337567297407,-0.6,0.25));
#32492=CARTESIAN_POINT('',(0.144337567297406,-0.96,0.25));
#32493=CARTESIAN_POINT('',(0.144337567297406,-0.6,0.25));
#32494=CARTESIAN_POINT('',(-0.144337567297407,-0.96,0.25));
#32495=CARTESIAN_POINT('Origin',(0.288675134594813,-0.6,0.));
#32496=CARTESIAN_POINT('',(0.144337567297406,-0.6,0.25));
#32497=CARTESIAN_POINT('',(0.144337567297406,-0.96,0.25));
#32498=CARTESIAN_POINT('Origin',(0.,-0.6,0.));
#32499=CARTESIAN_POINT('Origin',(0.,-0.96,0.));
#32698=UNCERTAINTY_MEASURE_WITH_UNIT(LENGTH_MEASURE(0.001),#32752,
'DISTANCE_ACCURACY_VALUE',
'Maximum model space distance between geometric entities at asserted c
onnectivities');
#32702=UNCERTAINTY_MEASURE_WITH_UNIT(LENGTH_MEASURE(0.001),#32752,
'DISTANCE_ACCURACY_VALUE',
'Maximum model space distance between geometric entities at asserted c
onnectivities');
#32747=(
GEOMETRIC_REPRESENTATION_CONTEXT(3)
GLOBAL_UNCERTAINTY_ASSIGNED_CONTEXT((#32698))
GLOBAL_UNIT_ASSIGNED_CONTEXT((#32752,#32754,#32755))
REPRESENTATION_CONTEXT('','3D')
);
#32751=(
GEOMETRIC_REPRESENTATION_CONTEXT(3)
GLOBAL_UNCERTAINTY_ASSIGNED_CONTEXT((#32702))
GLOBAL_UNIT_ASSIGNED_CONTEXT((#32752,#32754,#32755))
REPRESENTATION_CONTEXT('','3D')
);
#32752=(
LENGTH_UNIT()
NAMED_UNIT(*)
SI_UNIT(.CENTI.,.METRE.)
);
#32754=(
NAMED_UNIT(*)
PLANE_ANGLE_UNIT()
SI_UNIT($,.RADIAN.)
);
#32755=(
NAMED_UNIT(*)
SI_UNIT($,.STERADIAN.)
SOLID_ANGLE_UNIT()
);
#32800=SHAPE_DEFINITION_REPRESENTATION(#32857,#32973);
#32857=PRODUCT_DEFINITION_SHAPE('',$,#33022);
#32973=SHAPE_REPRESENTATION('',(#14025),#32747);
#32977=PRODUCT_DEFINITION_CONTEXT('part definition',#33123,'design');
#33022=PRODUCT_DEFINITION('Cap Screw - M6x25','Cap Screw - M6x25',#33070,
#32977);
#33070=PRODUCT_DEFINITION_FORMATION('',$,#33169);
#33123=APPLICATION_CONTEXT(
'Core Data for Automotive Mechanical Design Process');
#33124=PRODUCT_CONTEXT('part definition',#33123,'mechanical');
#33169=PRODUCT('Cap Screw - M6x25','Cap Screw - M6x25',
'Cap Screw - M6x25',(#33124));
#33243=COLOUR_RGB('Black',0.12,0.14,0.17);
#33244=FILL_AREA_STYLE_COLOUR('',#33243);
#33245=FILL_AREA_STYLE('',(#33244));
#33246=SURFACE_STYLE_FILL_AREA(#33245);
#33247=SURFACE_SIDE_STYLE('',(#33246));
#33248=SURFACE_STYLE_USAGE(.BOTH.,#33247);
#33249=PRESENTATION_STYLE_ASSIGNMENT((#33248));
ENDSEC;
END-ISO-10303-21;
